ISO-10303-21;
HEADER;
FILE_DESCRIPTION (('STEP AP214'),
    '1' );
FILE_NAME ('Contact Pads.step',
    '2026-10-07T17:53:07',
    ( '' ),
    ( '' ),
    'SwSTEP 2.0',
    'SolidWorks 2025',
    '' );
FILE_SCHEMA (( 'AUTOMOTIVE_DESIGN' ));
ENDSEC;

DATA;
#109=( LENGTH_UNIT ( ) NAMED_UNIT ( * ) SI_UNIT ( .MILLI., .METRE. ) );
#132=SURFACE_STYLE_FILL_AREA ( #10766 ) ;
#152=CARTESIAN_POINT ( 'NONE',  ( 5.999999999999999112, -12.00000000000000178, 7.000000000000000000 ) ) ;
#162=PRODUCT ( 'Contact Pads', 'Contact Pads', '', ( #11558 ) ) ;
#289=SURFACE_SIDE_STYLE ('',( #132 ) ) ;
#374=DIRECTION ( 'NONE',  ( 1.000000000000000000, 0.000000000000000000, 0.000000000000000000 ) ) ;
#403=DIRECTION ( 'NONE',  ( 0.000000000000000000, 1.000000000000000000, 0.000000000000000000 ) ) ;
#435=ORIENTED_EDGE ( 'NONE', *, *, #8093, .T. ) ;
#511=EDGE_CURVE ( 'NONE', #2084, #11003, #5649, .T. ) ;
#519=CARTESIAN_POINT ( 'NONE',  ( -6.000000000000000888, -12.00000000000000178, 0.000000000000000000 ) ) ;
#525=VERTEX_POINT ( 'NONE', #6502 ) ;
#608=PLANE ( 'NONE',  #5540 ) ;
#681=PRODUCT_DEFINITION_CONTEXT ( 'detailed design', #3608, 'design' ) ;
#745=DIRECTION ( 'NONE',  ( -0.000000000000000000, -0.000000000000000000, -1.000000000000000000 ) ) ;
#801=ADVANCED_FACE ( 'NONE', ( #1892 ), #7178, .F. ) ;
#812=STYLED_ITEM ( 'NONE', ( #8523 ), #8946 ) ;
#851=LINE ( 'NONE', #7260, #13582 ) ;
#858=ORIENTED_EDGE ( 'NONE', *, *, #13569, .T. ) ;
#937=EDGE_LOOP ( 'NONE', ( #8404, #3809, #12332, #11896 ) ) ;
#971=DIRECTION ( 'NONE',  ( -0.000000000000000000, -1.000000000000000000, -0.000000000000000000 ) ) ;
#1008=EDGE_CURVE ( 'NONE', #10778, #2084, #2802, .T. ) ;
#1028=CARTESIAN_POINT ( 'NONE',  ( 5.999999999999999112, 11.99999999999999822, 0.000000000000000000 ) ) ;
#1104=VECTOR ( 'NONE', #12608, 1000.000000000000000 ) ;
#1151=EDGE_CURVE ( 'NONE', #11003, #8866, #13588, .T. ) ;
#1337=ORIENTED_EDGE ( 'NONE', *, *, #10076, .F. ) ;
#1391=DIRECTION ( 'NONE',  ( 0.000000000000000000, 1.000000000000000000, 0.000000000000000000 ) ) ;
#1422=LINE ( 'NONE', #152, #10118 ) ;
#1443=APPLICATION_CONTEXT ( 'automotive_design' ) ;
#1752=ADVANCED_BREP_SHAPE_REPRESENTATION ( '', ( #8946, #6434 ), #2891 ) ;
#1782=VECTOR ( 'NONE', #374, 1000.000000000000000 ) ;
#1878=CARTESIAN_POINT ( 'NONE',  ( -6.000000000000000888, -12.00000000000000178, 0.000000000000000000 ) ) ;
#1892=FACE_OUTER_BOUND ( 'NONE', #6374, .T. ) ;
#1907=PLANE ( 'NONE',  #7309 ) ;
#2043=DIRECTION ( 'NONE',  ( 0.000000000000000000, -0.000000000000000000, -1.000000000000000000 ) ) ;
#2084=VERTEX_POINT ( 'NONE', #3906 ) ;
#2263=DIRECTION ( 'NONE',  ( -1.000000000000000000, -0.000000000000000000, -0.000000000000000000 ) ) ;
#2321=PRODUCT_DEFINITION_SHAPE ( 'NONE', 'NONE',  #9627 ) ;
#2448=SHAPE_REPRESENTATION_RELATIONSHIP ( 'NONE' , 'NONE' ,  #5156, #1752 ) ;
#2467=CARTESIAN_POINT ( 'NONE',  ( -6.000000000000000888, -12.00000000000000178, 7.000000000000000000 ) ) ;
#2480=AXIS2_PLACEMENT_3D ( 'NONE', #11287, #7151, #12547 ) ;
#2601=VECTOR ( 'NONE', #971, 1000.000000000000000 ) ;
#2633=LINE ( 'NONE', #519, #1782 ) ;
#2667=DIRECTION ( 'NONE',  ( 0.000000000000000000, -0.000000000000000000, 1.000000000000000000 ) ) ;
#2708=VECTOR ( 'NONE', #2263, 1000.000000000000000 ) ;
#2802=LINE ( 'NONE', #6959, #5814 ) ;
#2866=CARTESIAN_POINT ( 'NONE',  ( -6.000000000000000888, 11.99999999999999822, 7.000000000000000000 ) ) ;
#2869=EDGE_CURVE ( 'NONE', #12554, #525, #2633, .T. ) ;
#2891=( GEOMETRIC_REPRESENTATION_CONTEXT ( 3 ) GLOBAL_UNCERTAINTY_ASSIGNED_CONTEXT ( ( #11307 ) ) GLOBAL_UNIT_ASSIGNED_CONTEXT ( ( #109, #4323, #11084 ) ) REPRESENTATION_CONTEXT ( 'NONE', 'WORKASPACE' ) );
#3313=DIRECTION ( 'NONE',  ( -0.000000000000000000, -0.000000000000000000, -1.000000000000000000 ) ) ;
#3372=AXIS2_PLACEMENT_3D ( 'NONE', #11592, #10401, #2043 ) ;
#3513=ORIENTED_EDGE ( 'NONE', *, *, #5497, .T. ) ;
#3530=VECTOR ( 'NONE', #8695, 1000.000000000000000 ) ;
#3581=ADVANCED_FACE ( 'NONE', ( #9974 ), #6954, .T. ) ;
#3608=APPLICATION_CONTEXT ( 'automotive_design' ) ;
#3675=VERTEX_POINT ( 'NONE', #12142 ) ;
#3724=COLOUR_RGB ( '', 0.40784314, 0.44705882, 0.49803922) ;
#3809=ORIENTED_EDGE ( 'NONE', *, *, #5497, .F. ) ;
#3906=CARTESIAN_POINT ( 'NONE',  ( 5.999999999999999112, 11.99999999999999822, 7.000000000000000000 ) ) ;
#3953=FACE_OUTER_BOUND ( 'NONE', #4511, .T. ) ;
#4100=LINE ( 'NONE', #8347, #1104 ) ;
#4268=DIRECTION ( 'NONE',  ( -0.000000000000000000, -0.000000000000000000, -1.000000000000000000 ) ) ;
#4323=( NAMED_UNIT ( * ) PLANE_ANGLE_UNIT ( ) SI_UNIT ( $, .RADIAN. ) );
#4345=( NAMED_UNIT ( * ) SI_UNIT ( $, .STERADIAN. ) SOLID_ANGLE_UNIT ( ) );
#4449=ORIENTED_EDGE ( 'NONE', *, *, #6711, .F. ) ;
#4511=EDGE_LOOP ( 'NONE', ( #12424, #5714, #5015, #5780 ) ) ;
#4550=( LENGTH_UNIT ( ) NAMED_UNIT ( * ) SI_UNIT ( .MILLI., .METRE. ) );
#4590=EDGE_CURVE ( 'NONE', #3675, #12554, #8572, .T. ) ;
#4593=DIRECTION ( 'NONE',  ( 0.000000000000000000, 0.000000000000000000, -1.000000000000000000 ) ) ;
#4882=AXIS2_PLACEMENT_3D ( 'NONE', #2467, #1391, #2667 ) ;
#4911=FACE_OUTER_BOUND ( 'NONE', #9203, .T. ) ;
#5015=ORIENTED_EDGE ( 'NONE', *, *, #6711, .T. ) ;
#5104=ORIENTED_EDGE ( 'NONE', *, *, #7120, .F. ) ;
#5156=SHAPE_REPRESENTATION ( 'Contact Pads', ( #6434 ), #2891 ) ;
#5211=CARTESIAN_POINT ( 'NONE',  ( 5.999999999999999112, -12.00000000000000178, 7.000000000000000000 ) ) ;
#5231=ORIENTED_EDGE ( 'NONE', *, *, #4590, .F. ) ;
#5351=AXIS2_PLACEMENT_3D ( 'NONE', #12064, #4593, #8846 ) ;
#5370=CARTESIAN_POINT ( 'NONE',  ( -6.000000000000000888, 11.99999999999999822, 0.000000000000000000 ) ) ;
#5497=EDGE_CURVE ( 'NONE', #10778, #525, #1422, .T. ) ;
#5501=FILL_AREA_STYLE_COLOUR ( '', #3724 ) ;
#5540=AXIS2_PLACEMENT_3D ( 'NONE', #5700, #12286, #9981 ) ;
#5649=LINE ( 'NONE', #12915, #2708 ) ;
#5700=CARTESIAN_POINT ( 'NONE',  ( 5.999999999999999112, -12.00000000000000178, 7.000000000000000000 ) ) ;
#5714=ORIENTED_EDGE ( 'NONE', *, *, #511, .T. ) ;
#5780=ORIENTED_EDGE ( 'NONE', *, *, #9645, .T. ) ;
#5814=VECTOR ( 'NONE', #403, 1000.000000000000000 ) ;
#5911=CARTESIAN_POINT ( 'NONE',  ( 5.999999999999999112, -12.00000000000000178, 0.000000000000000000 ) ) ;
#6232=ORIENTED_EDGE ( 'NONE', *, *, #7120, .T. ) ;
#6237=LINE ( 'NONE', #10512, #11342 ) ;
#6374=EDGE_LOOP ( 'NONE', ( #6232, #10165, #7493, #6737 ) ) ;
#6434=AXIS2_PLACEMENT_3D ( 'NONE', #11654, #12825, #11856 ) ;
#6502=CARTESIAN_POINT ( 'NONE',  ( 5.999999999999999112, -12.00000000000000178, 0.000000000000000000 ) ) ;
#6562=ADVANCED_FACE ( 'NONE', ( #3953 ), #8203, .F. ) ;
#6608=LINE ( 'NONE', #13803, #2601 ) ;
#6711=EDGE_CURVE ( 'NONE', #11003, #3675, #4100, .T. ) ;
#6737=ORIENTED_EDGE ( 'NONE', *, *, #10076, .T. ) ;
#6954=PLANE ( 'NONE',  #5351 ) ;
#6959=CARTESIAN_POINT ( 'NONE',  ( 5.999999999999999112, -12.00000000000000178, 7.000000000000000000 ) ) ;
#7120=EDGE_CURVE ( 'NONE', #8048, #8866, #851, .T. ) ;
#7151=DIRECTION ( 'NONE',  ( 0.000000000000000000, 0.000000000000000000, -1.000000000000000000 ) ) ;
#7178=PLANE ( 'NONE',  #3372 ) ;
#7260=CARTESIAN_POINT ( 'NONE',  ( -6.000000000000000888, 11.99999999999999822, 0.000000000000000000 ) ) ;
#7309=AXIS2_PLACEMENT_3D ( 'NONE', #9175, #12384, #11334 ) ;
#7493=ORIENTED_EDGE ( 'NONE', *, *, #511, .F. ) ;
#7718=( GEOMETRIC_REPRESENTATION_CONTEXT ( 3 ) GLOBAL_UNCERTAINTY_ASSIGNED_CONTEXT ( ( #13396 ) ) GLOBAL_UNIT_ASSIGNED_CONTEXT ( ( #4550, #7737, #4345 ) ) REPRESENTATION_CONTEXT ( 'NONE', 'WORKASPACE' ) );
#7737=( NAMED_UNIT ( * ) PLANE_ANGLE_UNIT ( ) SI_UNIT ( $, .RADIAN. ) );
#7917=CARTESIAN_POINT ( 'NONE',  ( -6.000000000000000888, 11.99999999999999822, 7.000000000000000000 ) ) ;
#8048=VERTEX_POINT ( 'NONE', #1028 ) ;
#8093=EDGE_CURVE ( 'NONE', #8866, #12554, #6608, .T. ) ;
#8203=PLANE ( 'NONE',  #2480 ) ;
#8347=CARTESIAN_POINT ( 'NONE',  ( -6.000000000000000888, -12.00000000000000178, 7.000000000000000000 ) ) ;
#8403=DIRECTION ( 'NONE',  ( -0.000000000000000000, -0.000000000000000000, -1.000000000000000000 ) ) ;
#8404=ORIENTED_EDGE ( 'NONE', *, *, #2869, .T. ) ;
#8523=PRESENTATION_STYLE_ASSIGNMENT (( #12991 ) ) ;
#8572=LINE ( 'NONE', #11725, #9867 ) ;
#8695=DIRECTION ( 'NONE',  ( 1.000000000000000000, 0.000000000000000000, 0.000000000000000000 ) ) ;
#8785=ORIENTED_EDGE ( 'NONE', *, *, #8093, .F. ) ;
#8808=CLOSED_SHELL ( 'NONE', ( #10669, #801, #10399, #13700, #6562, #3581 ) ) ;
#8846=DIRECTION ( 'NONE',  ( -1.000000000000000000, 0.000000000000000000, -0.000000000000000000 ) ) ;
#8866=VERTEX_POINT ( 'NONE', #5370 ) ;
#8903=EDGE_LOOP ( 'NONE', ( #858, #1337, #13689, #3513 ) ) ;
#8946=MANIFOLD_SOLID_BREP ( 'Boss-Extrude1', #8808 ) ;
#9141=DIRECTION ( 'NONE',  ( 0.000000000000000000, 1.000000000000000000, 0.000000000000000000 ) ) ;
#9175=CARTESIAN_POINT ( 'NONE',  ( -6.000000000000000888, -12.00000000000000178, 7.000000000000000000 ) ) ;
#9203=EDGE_LOOP ( 'NONE', ( #435, #5231, #4449, #11783 ) ) ;
#9478=LINE ( 'NONE', #13722, #3530 ) ;
#9627=PRODUCT_DEFINITION ( 'UNKNOWN', '', #12025, #681 ) ;
#9645=EDGE_CURVE ( 'NONE', #3675, #10778, #9478, .T. ) ;
#9819=ORIENTED_EDGE ( 'NONE', *, *, #13569, .F. ) ;
#9867=VECTOR ( 'NONE', #4268, 1000.000000000000000 ) ;
#9974=FACE_OUTER_BOUND ( 'NONE', #13041, .T. ) ;
#9981=DIRECTION ( 'NONE',  ( 0.000000000000000000, 0.000000000000000000, 1.000000000000000000 ) ) ;
#10076=EDGE_CURVE ( 'NONE', #2084, #8048, #6237, .T. ) ;
#10087=VECTOR ( 'NONE', #745, 1000.000000000000000 ) ;
#10118=VECTOR ( 'NONE', #3313, 1000.000000000000000 ) ;
#10165=ORIENTED_EDGE ( 'NONE', *, *, #1151, .F. ) ;
#10312=SHAPE_DEFINITION_REPRESENTATION ( #2321, #5156 ) ;
#10399=ADVANCED_FACE ( 'NONE', ( #4911 ), #1907, .F. ) ;
#10401=DIRECTION ( 'NONE',  ( 0.000000000000000000, -1.000000000000000000, 0.000000000000000000 ) ) ;
#10512=CARTESIAN_POINT ( 'NONE',  ( 5.999999999999999112, 11.99999999999999822, 7.000000000000000000 ) ) ;
#10669=ADVANCED_FACE ( 'NONE', ( #11035 ), #608, .F. ) ;
#10766=FILL_AREA_STYLE ('',( #5501 ) ) ;
#10778=VERTEX_POINT ( 'NONE', #5211 ) ;
#11003=VERTEX_POINT ( 'NONE', #7917 ) ;
#11035=FACE_OUTER_BOUND ( 'NONE', #8903, .T. ) ;
#11040=LINE ( 'NONE', #5911, #13118 ) ;
#11084=( NAMED_UNIT ( * ) SI_UNIT ( $, .STERADIAN. ) SOLID_ANGLE_UNIT ( ) );
#11287=CARTESIAN_POINT ( 'NONE',  ( 0.000000000000000000, 0.000000000000000000, 7.000000000000000000 ) ) ;
#11307=UNCERTAINTY_MEASURE_WITH_UNIT (LENGTH_MEASURE( 1.000000000000000082E-05 ), #109, 'distance_accuracy_value', 'NONE');
#11334=DIRECTION ( 'NONE',  ( 0.000000000000000000, 0.000000000000000000, -1.000000000000000000 ) ) ;
#11342=VECTOR ( 'NONE', #8403, 1000.000000000000000 ) ;
#11558=PRODUCT_CONTEXT ( 'NONE', #1443, 'mechanical' ) ;
#11592=CARTESIAN_POINT ( 'NONE',  ( -6.000000000000000888, 11.99999999999999822, 7.000000000000000000 ) ) ;
#11654=CARTESIAN_POINT ( 'NONE',  ( 0.000000000000000000, 0.000000000000000000, 0.000000000000000000 ) ) ;
#11725=CARTESIAN_POINT ( 'NONE',  ( -6.000000000000000888, -12.00000000000000178, 7.000000000000000000 ) ) ;
#11783=ORIENTED_EDGE ( 'NONE', *, *, #1151, .T. ) ;
#11856=DIRECTION ( 'NONE',  ( 1.000000000000000000, 0.000000000000000000, 0.000000000000000000 ) ) ;
#11896=ORIENTED_EDGE ( 'NONE', *, *, #4590, .T. ) ;
#12025=PRODUCT_DEFINITION_FORMATION_WITH_SPECIFIED_SOURCE ( 'ANY', '', #162, .NOT_KNOWN. ) ;
#12064=CARTESIAN_POINT ( 'NONE',  ( 0.000000000000000000, 0.000000000000000000, 0.000000000000000000 ) ) ;
#12142=CARTESIAN_POINT ( 'NONE',  ( -6.000000000000000888, -12.00000000000000178, 7.000000000000000000 ) ) ;
#12286=DIRECTION ( 'NONE',  ( -1.000000000000000000, 0.000000000000000000, 0.000000000000000000 ) ) ;
#12332=ORIENTED_EDGE ( 'NONE', *, *, #9645, .F. ) ;
#12384=DIRECTION ( 'NONE',  ( 1.000000000000000000, 0.000000000000000000, 0.000000000000000000 ) ) ;
#12424=ORIENTED_EDGE ( 'NONE', *, *, #1008, .T. ) ;
#12547=DIRECTION ( 'NONE',  ( -1.000000000000000000, 0.000000000000000000, -0.000000000000000000 ) ) ;
#12554=VERTEX_POINT ( 'NONE', #1878 ) ;
#12608=DIRECTION ( 'NONE',  ( -0.000000000000000000, -1.000000000000000000, -0.000000000000000000 ) ) ;
#12825=DIRECTION ( 'NONE',  ( 0.000000000000000000, 0.000000000000000000, 1.000000000000000000 ) ) ;
#12915=CARTESIAN_POINT ( 'NONE',  ( -6.000000000000000888, 11.99999999999999822, 7.000000000000000000 ) ) ;
#12991=SURFACE_STYLE_USAGE ( .BOTH. , #289 ) ;
#13041=EDGE_LOOP ( 'NONE', ( #9819, #13075, #8785, #5104 ) ) ;
#13075=ORIENTED_EDGE ( 'NONE', *, *, #2869, .F. ) ;
#13117=FACE_OUTER_BOUND ( 'NONE', #937, .T. ) ;
#13118=VECTOR ( 'NONE', #9141, 1000.000000000000000 ) ;
#13394=PLANE ( 'NONE',  #4882 ) ;
#13396=UNCERTAINTY_MEASURE_WITH_UNIT (LENGTH_MEASURE( 1.000000000000000082E-05 ), #4550, 'distance_accuracy_value', 'NONE');
#13569=EDGE_CURVE ( 'NONE', #525, #8048, #11040, .T. ) ;
#13582=VECTOR ( 'NONE', #13698, 1000.000000000000000 ) ;
#13588=LINE ( 'NONE', #2866, #10087 ) ;
#13689=ORIENTED_EDGE ( 'NONE', *, *, #1008, .F. ) ;
#13698=DIRECTION ( 'NONE',  ( -1.000000000000000000, -0.000000000000000000, -0.000000000000000000 ) ) ;
#13700=ADVANCED_FACE ( 'NONE', ( #13117 ), #13394, .F. ) ;
#13722=CARTESIAN_POINT ( 'NONE',  ( -6.000000000000000888, -12.00000000000000178, 7.000000000000000000 ) ) ;
#13745=MECHANICAL_DESIGN_GEOMETRIC_PRESENTATION_REPRESENTATION('',(#812),#7718);
#13803=CARTESIAN_POINT ( 'NONE',  ( -6.000000000000000888, -12.00000000000000178, 0.000000000000000000 ) ) ;
ENDSEC;
END-ISO-10303-21;
